ISO-10303-21;
HEADER;
FILE_DESCRIPTION (('STEP AP214'),
    '1' );
FILE_NAME ('1.6 Slide Key.step',
    '2026-10-06T08:51:13',
    ( '' ),
    ( '' ),
    'SwSTEP 2.0',
    'SolidWorks 2021',
    '' );
FILE_SCHEMA (( 'AUTOMOTIVE_DESIGN' ));
ENDSEC;

DATA;
#2470=DIRECTION ( 'NONE',  ( -0.000000000000000000, -1.000000000000000000, -0.000000000000000000 ) ) ;
#2599=CARTESIAN_POINT ( 'NONE',  ( 2.000000000000000000, 2.375000000000000000, 1.069999999999998508 ) ) ;
#3068=EDGE_CURVE ( 'NONE', #90489, #14841, #61261, .T. ) ;
#3432=EDGE_CURVE ( 'NONE', #99331, #81879, #82118, .T. ) ;
#3668=CARTESIAN_POINT ( 'NONE',  ( -30.00000000000000355, 2.375000000000000000, -4.320000000000002061 ) ) ;
#4735=CARTESIAN_POINT ( 'NONE',  ( -2.000000000000000000, -2.375000000000000000, 4.319999999999998508 ) ) ;
#5235=DIRECTION ( 'NONE',  ( -1.000000000000000000, 0.000000000000000000, -0.000000000000000000 ) ) ;
#5485=EDGE_CURVE ( 'NONE', #90489, #118217, #82345, .T. ) ;
#5892=LINE ( 'NONE', #14668, #122730 ) ;
#6277=EDGE_CURVE ( 'NONE', #116174, #63949, #51319, .T. ) ;
#6643=ORIENTED_EDGE ( 'NONE', *, *, #3068, .F. ) ;
#6780=CARTESIAN_POINT ( 'NONE',  ( 2.000000000000000000, -2.375000000000000000, -0.000000000000000000 ) ) ;
#8331=UNCERTAINTY_MEASURE_WITH_UNIT (LENGTH_MEASURE( 1.000000000000000082E-05 ), #50018, 'distance_accuracy_value', 'NONE');
#8578=SHAPE_REPRESENTATION_RELATIONSHIP ( 'NONE' , 'NONE' ,  #9754, #74116 ) ;
#8925=CARTESIAN_POINT ( 'NONE',  ( 0.000000000000000000, 0.000000000000000000, 0.000000000000000000 ) ) ;
#9380=CARTESIAN_POINT ( 'NONE',  ( 0.000000000000000000, -2.375000000000000000, 4.319999999999998508 ) ) ;
#9406=EDGE_CURVE ( 'NONE', #63949, #99331, #130875, .T. ) ;
#9481=ORIENTED_EDGE ( 'NONE', *, *, #125888, .F. ) ;
#9754=SHAPE_REPRESENTATION ( '1.6 Slide Key', ( #127880 ), #121007 ) ;
#10005=PRODUCT_DEFINITION_SHAPE ( 'NONE', 'NONE',  #104142 ) ;
#10333=ORIENTED_EDGE ( 'NONE', *, *, #51376, .F. ) ;
#12071=ORIENTED_EDGE ( 'NONE', *, *, #60422, .F. ) ;
#12120=DIRECTION ( 'NONE',  ( -0.000000000000000000, -1.000000000000000000, -0.000000000000000000 ) ) ;
#12141=ADVANCED_FACE ( 'NONE', ( #15839 ), #39822, .T. ) ;
#12157=ORIENTED_EDGE ( 'NONE', *, *, #17062, .T. ) ;
#13292=APPLICATION_CONTEXT ( 'automotive_design' ) ;
#14454=LINE ( 'NONE', #123239, #120625 ) ;
#14668=CARTESIAN_POINT ( 'NONE',  ( -30.00000000000000355, -2.375000000000000000, 0.000000000000000000 ) ) ;
#14758=DIRECTION ( 'NONE',  ( 0.000000000000000000, 0.000000000000000000, 1.000000000000000000 ) ) ;
#14841=VERTEX_POINT ( 'NONE', #114366 ) ;
#15037=DIRECTION ( 'NONE',  ( 1.000000000000000000, -0.000000000000000000, 0.000000000000000000 ) ) ;
#15779=CARTESIAN_POINT ( 'NONE',  ( -30.00000000000000355, 2.375000000000000000, 0.000000000000000000 ) ) ;
#15839=FACE_OUTER_BOUND ( 'NONE', #123541, .T. ) ;
#15842=ORIENTED_EDGE ( 'NONE', *, *, #3432, .F. ) ;
#15948=EDGE_LOOP ( 'NONE', ( #79407, #27347, #71353, #102016 ) ) ;
#17036=SHAPE_DEFINITION_REPRESENTATION ( #10005, #9754 ) ;
#17062=EDGE_CURVE ( 'NONE', #123049, #90489, #78400, .T. ) ;
#17146=ADVANCED_FACE ( 'NONE', ( #123351 ), #91421, .F. ) ;
#17180=VERTEX_POINT ( 'NONE', #28307 ) ;
#17893=CARTESIAN_POINT ( 'NONE',  ( 29.99999999999999645, -2.375000000000000000, -4.320000000000002061 ) ) ;
#17922=DIRECTION ( 'NONE',  ( 0.000000000000000000, 0.000000000000000000, 1.000000000000000000 ) ) ;
#18554=ADVANCED_FACE ( 'NONE', ( #124740 ), #46524, .T. ) ;
#18710=CARTESIAN_POINT ( 'NONE',  ( 0.000000000000000000, 2.375000000000000000, 4.319999999999998508 ) ) ;
#19356=DIRECTION ( 'NONE',  ( 0.000000000000000000, 0.000000000000000000, -1.000000000000000000 ) ) ;
#19506=( NAMED_UNIT ( * ) PLANE_ANGLE_UNIT ( ) SI_UNIT ( $, .RADIAN. ) );
#20596=EDGE_CURVE ( 'NONE', #116174, #41627, #54734, .T. ) ;
#20825=CARTESIAN_POINT ( 'NONE',  ( -30.00000000000000355, 2.375000000000000000, 4.319999999999998508 ) ) ;
#21114=PRODUCT_DEFINITION_CONTEXT ( 'detailed design', #44916, 'design' ) ;
#21482=MECHANICAL_DESIGN_GEOMETRIC_PRESENTATION_REPRESENTATION('',(#107047),#123324);
#24864=AXIS2_PLACEMENT_3D ( 'NONE', #139116, #48525, #105039 ) ;
#25623=VECTOR ( 'NONE', #2470, 1000.000000000000000 ) ;
#25749=VECTOR ( 'NONE', #132871, 1000.000000000000000 ) ;
#26019=AXIS2_PLACEMENT_3D ( 'NONE', #15779, #64174, #140989 ) ;
#26044=UNCERTAINTY_MEASURE_WITH_UNIT (LENGTH_MEASURE( 1.000000000000000082E-05 ), #139461, 'distance_accuracy_value', 'NONE');
#26695=CARTESIAN_POINT ( 'NONE',  ( -2.000000000000000000, -2.375000000000000000, 1.069999999999998508 ) ) ;
#26995=DIRECTION ( 'NONE',  ( 1.000000000000000000, -0.000000000000000000, 0.000000000000000000 ) ) ;
#27347=ORIENTED_EDGE ( 'NONE', *, *, #5485, .F. ) ;
#27865=LINE ( 'NONE', #6780, #85447 ) ;
#28057=CARTESIAN_POINT ( 'NONE',  ( 2.000000000000000000, 2.375000000000000000, 1.069999999999998508 ) ) ;
#28307=CARTESIAN_POINT ( 'NONE',  ( -30.00000000000000355, -2.375000000000000000, 4.319999999999998508 ) ) ;
#29181=ORIENTED_EDGE ( 'NONE', *, *, #89204, .F. ) ;
#29549=EDGE_CURVE ( 'NONE', #78241, #123918, #43493, .T. ) ;
#30092=PLANE ( 'NONE',  #26019 ) ;
#30123=CARTESIAN_POINT ( 'NONE',  ( -2.000000000000000000, 2.375000000000000000, 1.069999999999998508 ) ) ;
#30979=CARTESIAN_POINT ( 'NONE',  ( 29.99999999999999645, -2.375000000000000000, 4.319999999999998508 ) ) ;
#31066=DIRECTION ( 'NONE',  ( -1.000000000000000000, 0.000000000000000000, -0.000000000000000000 ) ) ;
#31241=ORIENTED_EDGE ( 'NONE', *, *, #60422, .T. ) ;
#33020=UNCERTAINTY_MEASURE_WITH_UNIT (LENGTH_MEASURE( 1.000000000000000082E-05 ), #52138, 'distance_accuracy_value', 'NONE');
#33218=CARTESIAN_POINT ( 'NONE',  ( 29.99999999999999645, 2.375000000000000000, -4.320000000000002061 ) ) ;
#33695=CARTESIAN_POINT ( 'NONE',  ( 29.99999999999999645, -2.375000000000000000, -0.000000000000000000 ) ) ;
#33970=CARTESIAN_POINT ( 'NONE',  ( 0.000000000000000000, -2.375000000000000000, -4.320000000000002061 ) ) ;
#34248=CARTESIAN_POINT ( 'NONE',  ( -30.00000000000000355, 2.375000000000000000, -4.320000000000002061 ) ) ;
#34754=DIRECTION ( 'NONE',  ( 0.000000000000000000, 0.000000000000000000, 1.000000000000000000 ) ) ;
#35631=DIRECTION ( 'NONE',  ( 0.000000000000000000, 0.000000000000000000, -1.000000000000000000 ) ) ;
#35934=VECTOR ( 'NONE', #17922, 1000.000000000000000 ) ;
#35957=CARTESIAN_POINT ( 'NONE',  ( 29.99999999999999645, 2.375000000000000000, -4.320000000000002061 ) ) ;
#36469=PLANE ( 'NONE',  #61958 ) ;
#37161=LINE ( 'NONE', #124174, #84833 ) ;
#37257=PRESENTATION_STYLE_ASSIGNMENT (( #92322 ) ) ;
#37849=DIRECTION ( 'NONE',  ( 0.000000000000000000, 0.000000000000000000, 1.000000000000000000 ) ) ;
#37985=VECTOR ( 'NONE', #14758, 1000.000000000000000 ) ;
#39805=FACE_OUTER_BOUND ( 'NONE', #53376, .T. ) ;
#39822=PLANE ( 'NONE',  #24864 ) ;
#40399=LINE ( 'NONE', #138264, #126492 ) ;
#40566=( NAMED_UNIT ( * ) PLANE_ANGLE_UNIT ( ) SI_UNIT ( $, .RADIAN. ) );
#41105=FACE_OUTER_BOUND ( 'NONE', #99305, .T. ) ;
#41627=VERTEX_POINT ( 'NONE', #35957 ) ;
#42504=VERTEX_POINT ( 'NONE', #17893 ) ;
#43493=LINE ( 'NONE', #87708, #65354 ) ;
#43617=ORIENTED_EDGE ( 'NONE', *, *, #9406, .F. ) ;
#44023=CLOSED_SHELL ( 'NONE', ( #92436, #17146, #69405, #18554, #103238, #131894, #61088, #79794, #12141, #59177 ) ) ;
#44062=LINE ( 'NONE', #33218, #82357 ) ;
#44803=PRODUCT_DEFINITION_FORMATION_WITH_SPECIFIED_SOURCE ( 'ANY', '', #140743, .NOT_KNOWN. ) ;
#44916=APPLICATION_CONTEXT ( 'automotive_design' ) ;
#44966=CARTESIAN_POINT ( 'NONE',  ( -30.00000000000000355, 2.375000000000000000, 4.319999999999998508 ) ) ;
#45530=EDGE_CURVE ( 'NONE', #118158, #81879, #61177, .T. ) ;
#45952=EDGE_CURVE ( 'NONE', #17180, #81879, #139965, .T. ) ;
#46103=ORIENTED_EDGE ( 'NONE', *, *, #20596, .T. ) ;
#46160=ORIENTED_EDGE ( 'NONE', *, *, #70029, .F. ) ;
#46524=PLANE ( 'NONE',  #100639 ) ;
#46666=MANIFOLD_SOLID_BREP ( 'Boss-Extrude1', #44023 ) ;
#48525=DIRECTION ( 'NONE',  ( 0.000000000000000000, 1.000000000000000000, -0.000000000000000000 ) ) ;
#48632=EDGE_LOOP ( 'NONE', ( #82048, #71863, #73460, #31241 ) ) ;
#48928=DIRECTION ( 'NONE',  ( 0.000000000000000000, 0.000000000000000000, 1.000000000000000000 ) ) ;
#49441=AXIS2_PLACEMENT_3D ( 'NONE', #80556, #69692, #68971 ) ;
#49502=EDGE_CURVE ( 'NONE', #123049, #118158, #129437, .T. ) ;
#49691=PRODUCT_CONTEXT ( 'NONE', #13292, 'mechanical' ) ;
#50018=( LENGTH_UNIT ( ) NAMED_UNIT ( * ) SI_UNIT ( .MILLI., .METRE. ) );
#51319=LINE ( 'NONE', #117241, #35934 ) ;
#51345=LINE ( 'NONE', #20825, #111284 ) ;
#51376=EDGE_CURVE ( 'NONE', #121547, #17180, #5892, .T. ) ;
#51444=SURFACE_SIDE_STYLE ('',( #94908 ) ) ;
#52138=( LENGTH_UNIT ( ) NAMED_UNIT ( * ) SI_UNIT ( .MILLI., .METRE. ) );
#52191=EDGE_CURVE ( 'NONE', #118217, #66142, #27865, .T. ) ;
#52453=DIRECTION ( 'NONE',  ( 0.000000000000000000, 0.000000000000000000, 1.000000000000000000 ) ) ;
#52773=PLANE ( 'NONE',  #69879 ) ;
#53195=DIRECTION ( 'NONE',  ( 1.000000000000000000, 0.000000000000000000, 0.000000000000000000 ) ) ;
#53376=EDGE_LOOP ( 'NONE', ( #132601, #12071, #46103, #82765 ) ) ;
#53513=DIRECTION ( 'NONE',  ( -1.000000000000000000, 0.000000000000000000, -0.000000000000000000 ) ) ;
#53993=ORIENTED_EDGE ( 'NONE', *, *, #29549, .T. ) ;
#54402=DIRECTION ( 'NONE',  ( -0.000000000000000000, -1.000000000000000000, -0.000000000000000000 ) ) ;
#54734=LINE ( 'NONE', #76493, #66875 ) ;
#54953=CARTESIAN_POINT ( 'NONE',  ( 0.000000000000000000, 2.375000000000000000, -4.320000000000002061 ) ) ;
#55755=ORIENTED_EDGE ( 'NONE', *, *, #140199, .F. ) ;
#56938=DIRECTION ( 'NONE',  ( 1.000000000000000000, -0.000000000000000000, 0.000000000000000000 ) ) ;
#58988=FACE_OUTER_BOUND ( 'NONE', #15948, .T. ) ;
#59177=ADVANCED_FACE ( 'NONE', ( #61061 ), #62449, .F. ) ;
#59744=FILL_AREA_STYLE_COLOUR ( '', #108389 ) ;
#59805=CARTESIAN_POINT ( 'NONE',  ( -30.00000000000000355, -2.375000000000000000, -4.320000000000002061 ) ) ;
#59915=STYLED_ITEM ( 'NONE', ( #37257 ), #46666 ) ;
#60042=ORIENTED_EDGE ( 'NONE', *, *, #45952, .T. ) ;
#60387=DIRECTION ( 'NONE',  ( 0.000000000000000000, 0.000000000000000000, -1.000000000000000000 ) ) ;
#60422=EDGE_CURVE ( 'NONE', #116174, #121547, #90033, .T. ) ;
#60466=( NAMED_UNIT ( * ) PLANE_ANGLE_UNIT ( ) SI_UNIT ( $, .RADIAN. ) );
#61061=FACE_OUTER_BOUND ( 'NONE', #103427, .T. ) ;
#61088=ADVANCED_FACE ( 'NONE', ( #115878 ), #52773, .F. ) ;
#61128=VECTOR ( 'NONE', #133708, 1000.000000000000000 ) ;
#61177=LINE ( 'NONE', #69900, #37985 ) ;
#61261=LINE ( 'NONE', #95962, #111747 ) ;
#61958=AXIS2_PLACEMENT_3D ( 'NONE', #105969, #60387, #5235 ) ;
#62361=DIRECTION ( 'NONE',  ( -0.000000000000000000, -1.000000000000000000, -0.000000000000000000 ) ) ;
#62449=PLANE ( 'NONE',  #90222 ) ;
#62886=CARTESIAN_POINT ( 'NONE',  ( 0.000000000000000000, 2.375000000000000000, 4.319999999999998508 ) ) ;
#63497=ORIENTED_EDGE ( 'NONE', *, *, #3068, .T. ) ;
#63949=VERTEX_POINT ( 'NONE', #44966 ) ;
#64174=DIRECTION ( 'NONE',  ( 1.000000000000000000, 0.000000000000000000, 0.000000000000000000 ) ) ;
#64241=EDGE_CURVE ( 'NONE', #63949, #17180, #51345, .T. ) ;
#65354=VECTOR ( 'NONE', #54402, 1000.000000000000000 ) ;
#66142=VERTEX_POINT ( 'NONE', #141603 ) ;
#66875=VECTOR ( 'NONE', #132312, 1000.000000000000000 ) ;
#68971=DIRECTION ( 'NONE',  ( 0.000000000000000000, 0.000000000000000000, -1.000000000000000000 ) ) ;
#69405=ADVANCED_FACE ( 'NONE', ( #41105 ), #141874, .F. ) ;
#69692=DIRECTION ( 'NONE',  ( 1.000000000000000000, 0.000000000000000000, 0.000000000000000000 ) ) ;
#69879=AXIS2_PLACEMENT_3D ( 'NONE', #18710, #96261, #31066 ) ;
#69900=CARTESIAN_POINT ( 'NONE',  ( -2.000000000000000000, -2.375000000000000000, 0.000000000000000000 ) ) ;
#69986=ORIENTED_EDGE ( 'NONE', *, *, #82954, .T. ) ;
#70029=EDGE_CURVE ( 'NONE', #14841, #66142, #73235, .T. ) ;
#70228=CARTESIAN_POINT ( 'NONE',  ( -2.000000000000000000, 2.375000000000000000, 4.319999999999998508 ) ) ;
#70251=VECTOR ( 'NONE', #134951, 1000.000000000000000 ) ;
#71353=ORIENTED_EDGE ( 'NONE', *, *, #17062, .F. ) ;
#71763=FACE_OUTER_BOUND ( 'NONE', #109951, .T. ) ;
#71863=ORIENTED_EDGE ( 'NONE', *, *, #64241, .F. ) ;
#72066=SURFACE_STYLE_FILL_AREA ( #103905 ) ;
#73235=LINE ( 'NONE', #95671, #113257 ) ;
#73326=CARTESIAN_POINT ( 'NONE',  ( 0.000000000000000000, -2.375000000000000000, 0.000000000000000000 ) ) ;
#73363=CARTESIAN_POINT ( 'NONE',  ( -2.000000000000000000, 2.375000000000000000, 4.319999999999998508 ) ) ;
#73460=ORIENTED_EDGE ( 'NONE', *, *, #6277, .F. ) ;
#73949=ORIENTED_EDGE ( 'NONE', *, *, #64241, .T. ) ;
#74116=ADVANCED_BREP_SHAPE_REPRESENTATION ( '', ( #46666, #127880 ), #121007 ) ;
#74615=PLANE ( 'NONE',  #112009 ) ;
#75841=ORIENTED_EDGE ( 'NONE', *, *, #70029, .T. ) ;
#76006=ORIENTED_EDGE ( 'NONE', *, *, #81179, .T. ) ;
#76493=CARTESIAN_POINT ( 'NONE',  ( 0.000000000000000000, 2.375000000000000000, -4.320000000000002061 ) ) ;
#78241=VERTEX_POINT ( 'NONE', #116816 ) ;
#78400=LINE ( 'NONE', #88579, #70251 ) ;
#79407=ORIENTED_EDGE ( 'NONE', *, *, #136268, .T. ) ;
#79794=ADVANCED_FACE ( 'NONE', ( #71763 ), #74615, .T. ) ;
#80556=CARTESIAN_POINT ( 'NONE',  ( 2.000000000000000000, 2.375000000000000000, 0.000000000000000000 ) ) ;
#80723=MECHANICAL_DESIGN_GEOMETRIC_PRESENTATION_REPRESENTATION('',(#59915),#131631);
#81046=LINE ( 'NONE', #33970, #103308 ) ;
#81179=EDGE_CURVE ( 'NONE', #42504, #123918, #133016, .T. ) ;
#81569=EDGE_LOOP ( 'NONE', ( #60042, #15842, #43617, #73949 ) ) ;
#81738=ORIENTED_EDGE ( 'NONE', *, *, #91595, .F. ) ;
#81879=VERTEX_POINT ( 'NONE', #4735 ) ;
#82048=ORIENTED_EDGE ( 'NONE', *, *, #51376, .T. ) ;
#82118=LINE ( 'NONE', #73363, #141133 ) ;
#82307=ORIENTED_EDGE ( 'NONE', *, *, #52191, .T. ) ;
#82345=LINE ( 'NONE', #2599, #105737 ) ;
#82357=VECTOR ( 'NONE', #12120, 1000.000000000000000 ) ;
#82765=ORIENTED_EDGE ( 'NONE', *, *, #89204, .T. ) ;
#82954=EDGE_CURVE ( 'NONE', #66142, #123918, #14454, .T. ) ;
#83259=ORIENTED_EDGE ( 'NONE', *, *, #82954, .F. ) ;
#84771=( NAMED_UNIT ( * ) SI_UNIT ( $, .STERADIAN. ) SOLID_ANGLE_UNIT ( ) );
#84833=VECTOR ( 'NONE', #26995, 1000.000000000000000 ) ;
#84855=ORIENTED_EDGE ( 'NONE', *, *, #125888, .T. ) ;
#85447=VECTOR ( 'NONE', #48928, 1000.000000000000000 ) ;
#85533=DIRECTION ( 'NONE',  ( 1.000000000000000000, -0.000000000000000000, 0.000000000000000000 ) ) ;
#85638=VECTOR ( 'NONE', #56938, 1000.000000000000000 ) ;
#87708=CARTESIAN_POINT ( 'NONE',  ( 29.99999999999999645, 2.375000000000000000, 4.319999999999998508 ) ) ;
#88579=CARTESIAN_POINT ( 'NONE',  ( 0.000000000000000000, 2.375000000000000000, 1.069999999999998508 ) ) ;
#88843=LINE ( 'NONE', #135212, #85638 ) ;
#88901=VECTOR ( 'NONE', #85533, 1000.000000000000000 ) ;
#89204=EDGE_CURVE ( 'NONE', #41627, #42504, #44062, .T. ) ;
#89915=ORIENTED_EDGE ( 'NONE', *, *, #5485, .T. ) ;
#90033=LINE ( 'NONE', #34248, #25749 ) ;
#90222=AXIS2_PLACEMENT_3D ( 'NONE', #73326, #116805, #37849 ) ;
#90341=DIRECTION ( 'NONE',  ( -0.000000000000000000, -1.000000000000000000, -0.000000000000000000 ) ) ;
#90489=VERTEX_POINT ( 'NONE', #28057 ) ;
#90706=CARTESIAN_POINT ( 'NONE',  ( 29.99999999999999645, 2.375000000000000000, 0.000000000000000000 ) ) ;
#91421=PLANE ( 'NONE',  #49441 ) ;
#91557=EDGE_CURVE ( 'NONE', #121547, #42504, #81046, .T. ) ;
#91595=EDGE_CURVE ( 'NONE', #41627, #78241, #40399, .T. ) ;
#92322=SURFACE_STYLE_USAGE ( .BOTH. , #116240 ) ;
#92436=ADVANCED_FACE ( 'NONE', ( #58988 ), #36469, .F. ) ;
#94027=DIRECTION ( 'NONE',  ( 0.000000000000000000, 0.000000000000000000, 1.000000000000000000 ) ) ;
#94908=SURFACE_STYLE_FILL_AREA ( #107911 ) ;
#95533=DIRECTION ( 'NONE',  ( -0.000000000000000000, -1.000000000000000000, -0.000000000000000000 ) ) ;
#95671=CARTESIAN_POINT ( 'NONE',  ( 2.000000000000000000, 2.375000000000000000, 4.319999999999998508 ) ) ;
#95690=VECTOR ( 'NONE', #140991, 1000.000000000000000 ) ;
#95962=CARTESIAN_POINT ( 'NONE',  ( 2.000000000000000000, 2.375000000000000000, 0.000000000000000000 ) ) ;
#96261=DIRECTION ( 'NONE',  ( 0.000000000000000000, 0.000000000000000000, -1.000000000000000000 ) ) ;
#96746=CARTESIAN_POINT ( 'NONE',  ( 0.000000000000000000, 2.375000000000000000, 4.319999999999998508 ) ) ;
#97485=FACE_OUTER_BOUND ( 'NONE', #48632, .T. ) ;
#99305=EDGE_LOOP ( 'NONE', ( #69986, #132127, #55755, #75841 ) ) ;
#99331=VERTEX_POINT ( 'NONE', #70228 ) ;
#100639=AXIS2_PLACEMENT_3D ( 'NONE', #90706, #134943, #35631 ) ;
#101558=EDGE_LOOP ( 'NONE', ( #82307, #46160, #6643, #89915 ) ) ;
#102016=ORIENTED_EDGE ( 'NONE', *, *, #49502, .T. ) ;
#102246=ORIENTED_EDGE ( 'NONE', *, *, #136268, .F. ) ;
#102524=COLOUR_RGB ( '', 0.72549020, 0.75294118, 0.79215686) ;
#102729=AXIS2_PLACEMENT_3D ( 'NONE', #54953, #131069, #53513 ) ;
#102985=ORIENTED_EDGE ( 'NONE', *, *, #91595, .T. ) ;
#103238=ADVANCED_FACE ( 'NONE', ( #39805 ), #119445, .T. ) ;
#103308=VECTOR ( 'NONE', #15037, 1000.000000000000000 ) ;
#103427=EDGE_LOOP ( 'NONE', ( #102246, #136279, #132279, #10333, #135431, #76006, #83259, #140281 ) ) ;
#103905=FILL_AREA_STYLE ('',( #59744 ) ) ;
#104142=PRODUCT_DEFINITION ( 'UNKNOWN', '', #44803, #21114 ) ;
#105039=DIRECTION ( 'NONE',  ( 0.000000000000000000, 0.000000000000000000, 1.000000000000000000 ) ) ;
#105737=VECTOR ( 'NONE', #90341, 1000.000000000000000 ) ;
#105969=CARTESIAN_POINT ( 'NONE',  ( 0.000000000000000000, 2.375000000000000000, 1.069999999999998508 ) ) ;
#107047=STYLED_ITEM ( 'NONE', ( #116680 ), #74116 ) ;
#107911=FILL_AREA_STYLE ('',( #127563 ) ) ;
#108240=ORIENTED_EDGE ( 'NONE', *, *, #6277, .T. ) ;
#108389=COLOUR_RGB ( '', 0.72549020, 0.75294118, 0.79215686) ;
#108435=EDGE_LOOP ( 'NONE', ( #131719, #29181, #102985, #53993 ) ) ;
#108490=CARTESIAN_POINT ( 'NONE',  ( 2.000000000000000000, -2.375000000000000000, 1.069999999999998508 ) ) ;
#109951=EDGE_LOOP ( 'NONE', ( #118762, #129934, #84855, #120232 ) ) ;
#111284=VECTOR ( 'NONE', #95533, 1000.000000000000000 ) ;
#111747=VECTOR ( 'NONE', #52453, 1000.000000000000000 ) ;
#112009=AXIS2_PLACEMENT_3D ( 'NONE', #128971, #118804, #115924 ) ;
#112413=ORIENTED_EDGE ( 'NONE', *, *, #20596, .F. ) ;
#113257=VECTOR ( 'NONE', #62361, 1000.000000000000000 ) ;
#114366=CARTESIAN_POINT ( 'NONE',  ( 2.000000000000000000, 2.375000000000000000, 4.319999999999998508 ) ) ;
#115398=AXIS2_PLACEMENT_3D ( 'NONE', #62886, #19356, #142578 ) ;
#115878=FACE_OUTER_BOUND ( 'NONE', #81569, .T. ) ;
#115924=DIRECTION ( 'NONE',  ( 0.000000000000000000, 0.000000000000000000, -1.000000000000000000 ) ) ;
#116174=VERTEX_POINT ( 'NONE', #3668 ) ;
#116240=SURFACE_SIDE_STYLE ('',( #72066 ) ) ;
#116680=PRESENTATION_STYLE_ASSIGNMENT (( #128287 ) ) ;
#116805=DIRECTION ( 'NONE',  ( 0.000000000000000000, 1.000000000000000000, -0.000000000000000000 ) ) ;
#116816=CARTESIAN_POINT ( 'NONE',  ( 29.99999999999999645, 2.375000000000000000, 4.319999999999998508 ) ) ;
#117241=CARTESIAN_POINT ( 'NONE',  ( -30.00000000000000355, 2.375000000000000000, 0.000000000000000000 ) ) ;
#118158=VERTEX_POINT ( 'NONE', #26695 ) ;
#118217=VERTEX_POINT ( 'NONE', #108490 ) ;
#118762=ORIENTED_EDGE ( 'NONE', *, *, #45530, .F. ) ;
#118804=DIRECTION ( 'NONE',  ( 1.000000000000000000, 0.000000000000000000, 0.000000000000000000 ) ) ;
#118816=( NAMED_UNIT ( * ) SI_UNIT ( $, .STERADIAN. ) SOLID_ANGLE_UNIT ( ) );
#119445=PLANE ( 'NONE',  #102729 ) ;
#120232=ORIENTED_EDGE ( 'NONE', *, *, #3432, .T. ) ;
#120625=VECTOR ( 'NONE', #134103, 1000.000000000000000 ) ;
#121007=( GEOMETRIC_REPRESENTATION_CONTEXT ( 3 ) GLOBAL_UNCERTAINTY_ASSIGNED_CONTEXT ( ( #33020 ) ) GLOBAL_UNIT_ASSIGNED_CONTEXT ( ( #52138, #40566, #118816 ) ) REPRESENTATION_CONTEXT ( 'NONE', 'WORKASPACE' ) );
#121547=VERTEX_POINT ( 'NONE', #59805 ) ;
#122730=VECTOR ( 'NONE', #136432, 1000.000000000000000 ) ;
#123049=VERTEX_POINT ( 'NONE', #143079 ) ;
#123239=CARTESIAN_POINT ( 'NONE',  ( 0.000000000000000000, -2.375000000000000000, 4.319999999999998508 ) ) ;
#123324=( GEOMETRIC_REPRESENTATION_CONTEXT ( 3 ) GLOBAL_UNCERTAINTY_ASSIGNED_CONTEXT ( ( #8331 ) ) GLOBAL_UNIT_ASSIGNED_CONTEXT ( ( #50018, #19506, #84771 ) ) REPRESENTATION_CONTEXT ( 'NONE', 'WORKASPACE' ) );
#123351=FACE_OUTER_BOUND ( 'NONE', #101558, .T. ) ;
#123541=EDGE_LOOP ( 'NONE', ( #12157, #63497, #135885, #81738, #112413, #108240, #124006, #9481 ) ) ;
#123918=VERTEX_POINT ( 'NONE', #30979 ) ;
#124006=ORIENTED_EDGE ( 'NONE', *, *, #9406, .T. ) ;
#124174=CARTESIAN_POINT ( 'NONE',  ( 0.000000000000000000, -2.375000000000000000, 1.069999999999998508 ) ) ;
#124602=CARTESIAN_POINT ( 'NONE',  ( -2.000000000000000000, 2.375000000000000000, 0.000000000000000000 ) ) ;
#124740=FACE_OUTER_BOUND ( 'NONE', #108435, .T. ) ;
#125888=EDGE_CURVE ( 'NONE', #123049, #99331, #134065, .T. ) ;
#126294=DIRECTION ( 'NONE',  ( -0.000000000000000000, -1.000000000000000000, -0.000000000000000000 ) ) ;
#126492=VECTOR ( 'NONE', #94027, 1000.000000000000000 ) ;
#127563=FILL_AREA_STYLE_COLOUR ( '', #102524 ) ;
#127853=( NAMED_UNIT ( * ) SI_UNIT ( $, .STERADIAN. ) SOLID_ANGLE_UNIT ( ) );
#127880=AXIS2_PLACEMENT_3D ( 'NONE', #8925, #141658, #53195 ) ;
#128287=SURFACE_STYLE_USAGE ( .BOTH. , #51444 ) ;
#128971=CARTESIAN_POINT ( 'NONE',  ( -2.000000000000000000, 2.375000000000000000, 0.000000000000000000 ) ) ;
#129437=LINE ( 'NONE', #30123, #25623 ) ;
#129934=ORIENTED_EDGE ( 'NONE', *, *, #49502, .F. ) ;
#130875=LINE ( 'NONE', #96746, #95690 ) ;
#131069=DIRECTION ( 'NONE',  ( 0.000000000000000000, 0.000000000000000000, -1.000000000000000000 ) ) ;
#131631=( GEOMETRIC_REPRESENTATION_CONTEXT ( 3 ) GLOBAL_UNCERTAINTY_ASSIGNED_CONTEXT ( ( #26044 ) ) GLOBAL_UNIT_ASSIGNED_CONTEXT ( ( #139461, #60466, #127853 ) ) REPRESENTATION_CONTEXT ( 'NONE', 'WORKASPACE' ) );
#131719=ORIENTED_EDGE ( 'NONE', *, *, #81179, .F. ) ;
#131894=ADVANCED_FACE ( 'NONE', ( #97485 ), #30092, .F. ) ;
#132127=ORIENTED_EDGE ( 'NONE', *, *, #29549, .F. ) ;
#132279=ORIENTED_EDGE ( 'NONE', *, *, #45952, .F. ) ;
#132312=DIRECTION ( 'NONE',  ( 1.000000000000000000, -0.000000000000000000, 0.000000000000000000 ) ) ;
#132601=ORIENTED_EDGE ( 'NONE', *, *, #91557, .F. ) ;
#132871=DIRECTION ( 'NONE',  ( -0.000000000000000000, -1.000000000000000000, -0.000000000000000000 ) ) ;
#133016=LINE ( 'NONE', #33695, #61128 ) ;
#133708=DIRECTION ( 'NONE',  ( 0.000000000000000000, 0.000000000000000000, 1.000000000000000000 ) ) ;
#134065=LINE ( 'NONE', #124602, #143182 ) ;
#134103=DIRECTION ( 'NONE',  ( 1.000000000000000000, -0.000000000000000000, 0.000000000000000000 ) ) ;
#134943=DIRECTION ( 'NONE',  ( 1.000000000000000000, 0.000000000000000000, 0.000000000000000000 ) ) ;
#134951=DIRECTION ( 'NONE',  ( 1.000000000000000000, -0.000000000000000000, 0.000000000000000000 ) ) ;
#135212=CARTESIAN_POINT ( 'NONE',  ( 0.000000000000000000, 2.375000000000000000, 4.319999999999998508 ) ) ;
#135431=ORIENTED_EDGE ( 'NONE', *, *, #91557, .T. ) ;
#135885=ORIENTED_EDGE ( 'NONE', *, *, #140199, .T. ) ;
#136268=EDGE_CURVE ( 'NONE', #118158, #118217, #37161, .T. ) ;
#136279=ORIENTED_EDGE ( 'NONE', *, *, #45530, .T. ) ;
#136432=DIRECTION ( 'NONE',  ( 0.000000000000000000, 0.000000000000000000, 1.000000000000000000 ) ) ;
#138264=CARTESIAN_POINT ( 'NONE',  ( 29.99999999999999645, 2.375000000000000000, 0.000000000000000000 ) ) ;
#139116=CARTESIAN_POINT ( 'NONE',  ( 0.000000000000000000, 2.375000000000000000, 0.000000000000000000 ) ) ;
#139461=( LENGTH_UNIT ( ) NAMED_UNIT ( * ) SI_UNIT ( .MILLI., .METRE. ) );
#139965=LINE ( 'NONE', #9380, #88901 ) ;
#140199=EDGE_CURVE ( 'NONE', #14841, #78241, #88843, .T. ) ;
#140281=ORIENTED_EDGE ( 'NONE', *, *, #52191, .F. ) ;
#140743=PRODUCT ( '1.6 Slide Key', '1.6 Slide Key', '', ( #49691 ) ) ;
#140989=DIRECTION ( 'NONE',  ( 0.000000000000000000, 0.000000000000000000, -1.000000000000000000 ) ) ;
#140991=DIRECTION ( 'NONE',  ( 1.000000000000000000, -0.000000000000000000, 0.000000000000000000 ) ) ;
#141133=VECTOR ( 'NONE', #126294, 1000.000000000000000 ) ;
#141603=CARTESIAN_POINT ( 'NONE',  ( 2.000000000000000000, -2.375000000000000000, 4.319999999999998508 ) ) ;
#141658=DIRECTION ( 'NONE',  ( 0.000000000000000000, 0.000000000000000000, 1.000000000000000000 ) ) ;
#141874=PLANE ( 'NONE',  #115398 ) ;
#142578=DIRECTION ( 'NONE',  ( -1.000000000000000000, 0.000000000000000000, -0.000000000000000000 ) ) ;
#143079=CARTESIAN_POINT ( 'NONE',  ( -2.000000000000000000, 2.375000000000000000, 1.069999999999998508 ) ) ;
#143182=VECTOR ( 'NONE', #34754, 1000.000000000000000 ) ;
ENDSEC;
END-ISO-10303-21;
